ISO-10303-21;
HEADER;
/* Generated by software containing ST-Developer
 * from STEP Tools, Inc. (www.steptools.com) 
 */

FILE_DESCRIPTION(
/* description */ ('PAT-091'),
/* implementation_level */ '2;1');

FILE_NAME(
/* name */ 'Axle distance sleeve 5 mm (2).step',
/* time_stamp */ '2026-10-27T15:34:44-07:00',
/* author */ (''),
/* organization */ (''),
/* preprocessor_version */ 'ST-DEVELOPER v20.2',
/* originating_system */ 'Autodesk Translation Framework v15.17.0.0',
/* authorisation */ '');

FILE_SCHEMA (('AUTOMOTIVE_DESIGN { 1 0 10303 214 3 1 1 }'));
ENDSEC;

DATA;
#10=MECHANICAL_DESIGN_GEOMETRIC_PRESENTATION_REPRESENTATION('',(#997),#25100);
#777=SHAPE_REPRESENTATION_RELATIONSHIP('SRR','None',#25539,#887);
#887=ADVANCED_BREP_SHAPE_REPRESENTATION('',(#1120),#25009);
#997=STYLED_ITEM('',(#26191),#1120);
#1120=MANIFOLD_SOLID_BREP('Body1',#13275);
#1383=FACE_BOUND('',#3279,.T.);
#1384=FACE_BOUND('',#3281,.T.);
#1758=PLANE('',#15063);
#1759=PLANE('',#15064);
#2290=FACE_OUTER_BOUND('',#3276,.T.);
#2291=FACE_OUTER_BOUND('',#3277,.T.);
#2292=FACE_OUTER_BOUND('',#3278,.T.);
#2293=FACE_OUTER_BOUND('',#3280,.T.);
#3276=EDGE_LOOP('',(#9944,#9945,#9946,#9947));
#3277=EDGE_LOOP('',(#9948,#9949,#9950,#9951));
#3278=EDGE_LOOP('',(#9952));
#3279=EDGE_LOOP('',(#9953));
#3280=EDGE_LOOP('',(#9954));
#3281=EDGE_LOOP('',(#9955));
#4395=LINE('',#22044,#5135);
#4396=LINE('',#22050,#5136);
#5135=VECTOR('',#17687,0.605);
#5136=VECTOR('',#17694,0.8);
#5819=CIRCLE('',#15058,0.605);
#5820=CIRCLE('',#15059,0.605);
#5821=CIRCLE('',#15061,0.8);
#5822=CIRCLE('',#15062,0.8);
#6706=VERTEX_POINT('',#22041);
#6707=VERTEX_POINT('',#22043);
#6708=VERTEX_POINT('',#22047);
#6709=VERTEX_POINT('',#22049);
#7907=EDGE_CURVE('',#6706,#6706,#5819,.T.);
#7908=EDGE_CURVE('',#6706,#6707,#4395,.T.);
#7909=EDGE_CURVE('',#6707,#6707,#5820,.T.);
#7910=EDGE_CURVE('',#6708,#6708,#5821,.T.);
#7911=EDGE_CURVE('',#6708,#6709,#4396,.T.);
#7912=EDGE_CURVE('',#6709,#6709,#5822,.T.);
#9944=ORIENTED_EDGE('',*,*,#7907,.F.);
#9945=ORIENTED_EDGE('',*,*,#7908,.T.);
#9946=ORIENTED_EDGE('',*,*,#7909,.T.);
#9947=ORIENTED_EDGE('',*,*,#7908,.F.);
#9948=ORIENTED_EDGE('',*,*,#7910,.F.);
#9949=ORIENTED_EDGE('',*,*,#7911,.T.);
#9950=ORIENTED_EDGE('',*,*,#7912,.T.);
#9951=ORIENTED_EDGE('',*,*,#7911,.F.);
#9952=ORIENTED_EDGE('',*,*,#7910,.T.);
#9953=ORIENTED_EDGE('',*,*,#7907,.T.);
#9954=ORIENTED_EDGE('',*,*,#7912,.F.);
#9955=ORIENTED_EDGE('',*,*,#7909,.F.);
#12180=CYLINDRICAL_SURFACE('',#15057,0.605);
#12181=CYLINDRICAL_SURFACE('',#15060,0.8);
#12657=ADVANCED_FACE('',(#2290),#12180,.F.);
#12658=ADVANCED_FACE('',(#2291),#12181,.T.);
#12659=ADVANCED_FACE('',(#2292,#1383),#1758,.T.);
#12660=ADVANCED_FACE('',(#2293,#1384),#1759,.F.);
#13275=CLOSED_SHELL('',(#12657,#12658,#12659,#12660));
#15056=AXIS2_PLACEMENT_3D('',#22039,#17681,#17682);
#15057=AXIS2_PLACEMENT_3D('',#22040,#17683,#17684);
#15058=AXIS2_PLACEMENT_3D('',#22042,#17685,#17686);
#15059=AXIS2_PLACEMENT_3D('',#22045,#17688,#17689);
#15060=AXIS2_PLACEMENT_3D('',#22046,#17690,#17691);
#15061=AXIS2_PLACEMENT_3D('',#22048,#17692,#17693);
#15062=AXIS2_PLACEMENT_3D('',#22051,#17695,#17696);
#15063=AXIS2_PLACEMENT_3D('',#22052,#17697,#17698);
#15064=AXIS2_PLACEMENT_3D('',#22053,#17699,#17700);
#17681=DIRECTION('axis',(0.,0.,1.));
#17682=DIRECTION('refdir',(1.,0.,0.));
#17683=DIRECTION('center_axis',(0.,1.,0.));
#17684=DIRECTION('ref_axis',(1.,0.,0.));
#17685=DIRECTION('center_axis',(0.,-1.,0.));
#17686=DIRECTION('ref_axis',(1.,0.,0.));
#17687=DIRECTION('',(0.,-1.,0.));
#17688=DIRECTION('center_axis',(0.,-1.,0.));
#17689=DIRECTION('ref_axis',(1.,0.,0.));
#17690=DIRECTION('center_axis',(0.,1.,0.));
#17691=DIRECTION('ref_axis',(1.,0.,0.));
#17692=DIRECTION('center_axis',(0.,1.,0.));
#17693=DIRECTION('ref_axis',(1.,0.,0.));
#17694=DIRECTION('',(0.,-1.,0.));
#17695=DIRECTION('center_axis',(0.,1.,0.));
#17696=DIRECTION('ref_axis',(1.,0.,0.));
#17697=DIRECTION('center_axis',(0.,1.,0.));
#17698=DIRECTION('ref_axis',(1.,0.,0.));
#17699=DIRECTION('center_axis',(0.,1.,0.));
#17700=DIRECTION('ref_axis',(1.,0.,0.));
#22039=CARTESIAN_POINT('',(0.,0.,0.));
#22040=CARTESIAN_POINT('Origin',(0.,-6.,13.));
#22041=CARTESIAN_POINT('',(-0.605,-5.5,13.));
#22042=CARTESIAN_POINT('Origin',(0.,-5.5,13.));
#22043=CARTESIAN_POINT('',(-0.605,-6.,13.));
#22044=CARTESIAN_POINT('',(-0.605,-6.,13.));
#22045=CARTESIAN_POINT('Origin',(0.,-6.,13.));
#22046=CARTESIAN_POINT('Origin',(0.,-6.,13.));
#22047=CARTESIAN_POINT('',(-0.8,-5.5,13.));
#22048=CARTESIAN_POINT('Origin',(0.,-5.5,13.));
#22049=CARTESIAN_POINT('',(-0.8,-6.,13.));
#22050=CARTESIAN_POINT('',(-0.8,-6.,13.));
#22051=CARTESIAN_POINT('Origin',(0.,-6.,13.));
#22052=CARTESIAN_POINT('Origin',(0.,-5.5,13.));
#22053=CARTESIAN_POINT('Origin',(0.,-6.,13.));
#24888=UNCERTAINTY_MEASURE_WITH_UNIT(LENGTH_MEASURE(0.001),#25101,
'DISTANCE_ACCURACY_VALUE',
'Maximum model space distance between geometric entities at asserted c
onnectivities');
#24979=UNCERTAINTY_MEASURE_WITH_UNIT(LENGTH_MEASURE(0.001),#25101,
'DISTANCE_ACCURACY_VALUE',
'Maximum model space distance between geometric entities at asserted c
onnectivities');
#25009=(
GEOMETRIC_REPRESENTATION_CONTEXT(3)
GLOBAL_UNCERTAINTY_ASSIGNED_CONTEXT((#24888))
GLOBAL_UNIT_ASSIGNED_CONTEXT((#25101,#25103,#25104))
REPRESENTATION_CONTEXT('','3D')
);
#25100=(
GEOMETRIC_REPRESENTATION_CONTEXT(3)
GLOBAL_UNCERTAINTY_ASSIGNED_CONTEXT((#24979))
GLOBAL_UNIT_ASSIGNED_CONTEXT((#25101,#25103,#25104))
REPRESENTATION_CONTEXT('','3D')
);
#25101=(
LENGTH_UNIT()
NAMED_UNIT(*)
SI_UNIT(.CENTI.,.METRE.)
);
#25103=(
NAMED_UNIT(*)
PLANE_ANGLE_UNIT()
SI_UNIT($,.RADIAN.)
);
#25104=(
NAMED_UNIT(*)
SI_UNIT($,.STERADIAN.)
SOLID_ANGLE_UNIT()
);
#25134=SHAPE_DEFINITION_REPRESENTATION(#25254,#25539);
#25254=PRODUCT_DEFINITION_SHAPE('',$,#25660);
#25539=SHAPE_REPRESENTATION('',(#15056),#25009);
#25630=PRODUCT_DEFINITION_CONTEXT('part definition',#25992,'design');
#25660=PRODUCT_DEFINITION('Axle distance sleeve 5 mm (2)',
'Axle distance sleeve 5 mm (2)',#25780,#25630);
#25780=PRODUCT_DEFINITION_FORMATION('',$,#26023);
#25992=APPLICATION_CONTEXT(
'Core Data for Automotive Mechanical Design Process');
#25993=PRODUCT_CONTEXT('part definition',#25992,'mechanical');
#26023=PRODUCT('Axle distance sleeve 5 mm (2)',
'Axle distance sleeve 5 mm (2)','Axle distance sleeve 5 mm (2)',(#25993));
#26185=COLOUR_RGB('Grey',0.48,0.52,0.57);
#26186=FILL_AREA_STYLE_COLOUR('',#26185);
#26187=FILL_AREA_STYLE('',(#26186));
#26188=SURFACE_STYLE_FILL_AREA(#26187);
#26189=SURFACE_SIDE_STYLE('',(#26188));
#26190=SURFACE_STYLE_USAGE(.BOTH.,#26189);
#26191=PRESENTATION_STYLE_ASSIGNMENT((#26190));
ENDSEC;
END-ISO-10303-21;
